ISO-10303-21;
HEADER;
/* Generated by software containing ST-Developer
 * from STEP Tools, Inc. (www.steptools.com) 
 */

FILE_DESCRIPTION(
/* description */ ('Crank-driven oscillating fan base (mechanism only)'),

/* implementation_level */ '2;1');

FILE_NAME(
/* name */ 'Socket Set Screw - M4x6.step',
/* time_stamp */ '2026-10-28T03:25:00-07:00',
/* author */ (''),
/* organization */ (''),
/* preprocessor_version */ 'ST-DEVELOPER v20.2',
/* originating_system */ 'Autodesk Translation Framework v15.17.0.0',
/* authorisation */ '');

FILE_SCHEMA (('AUTOMOTIVE_DESIGN { 1 0 10303 214 3 1 1 }'));
ENDSEC;

DATA;
#10=MECHANICAL_DESIGN_GEOMETRIC_PRESENTATION_REPRESENTATION('',(#470),#11916);
#300=CONICAL_SURFACE('',#7117,0.185,0.785398163397449);
#301=CONICAL_SURFACE('',#7121,0.1625,0.785398163397449);
#382=SHAPE_REPRESENTATION_RELATIONSHIP('SRR','None',#12108,#422);
#422=ADVANCED_BREP_SHAPE_REPRESENTATION('',(#517),#11899);
#470=STYLED_ITEM('',(#12382),#517);
#517=MANIFOLD_SOLID_BREP('Body1',#6101);
#648=FACE_BOUND('',#1630,.T.);
#806=PLANE('',#7108);
#807=PLANE('',#7109);
#808=PLANE('',#7110);
#809=PLANE('',#7111);
#810=PLANE('',#7112);
#811=PLANE('',#7113);
#812=PLANE('',#7114);
#813=PLANE('',#7115);
#814=PLANE('',#7123);
#1129=FACE_OUTER_BOUND('',#1622,.T.);
#1130=FACE_OUTER_BOUND('',#1623,.T.);
#1131=FACE_OUTER_BOUND('',#1624,.T.);
#1132=FACE_OUTER_BOUND('',#1625,.T.);
#1133=FACE_OUTER_BOUND('',#1626,.T.);
#1134=FACE_OUTER_BOUND('',#1627,.T.);
#1135=FACE_OUTER_BOUND('',#1628,.T.);
#1136=FACE_OUTER_BOUND('',#1629,.T.);
#1137=FACE_OUTER_BOUND('',#1631,.T.);
#1138=FACE_OUTER_BOUND('',#1632,.T.);
#1139=FACE_OUTER_BOUND('',#1633,.T.);
#1140=FACE_OUTER_BOUND('',#1634,.T.);
#1622=EDGE_LOOP('',(#5048,#5049,#5050,#5051));
#1623=EDGE_LOOP('',(#5052,#5053,#5054,#5055));
#1624=EDGE_LOOP('',(#5056,#5057,#5058,#5059));
#1625=EDGE_LOOP('',(#5060,#5061,#5062,#5063));
#1626=EDGE_LOOP('',(#5064,#5065,#5066,#5067));
#1627=EDGE_LOOP('',(#5068,#5069,#5070,#5071));
#1628=EDGE_LOOP('',(#5072,#5073,#5074,#5075,#5076,#5077));
#1629=EDGE_LOOP('',(#5078));
#1630=EDGE_LOOP('',(#5079,#5080,#5081,#5082,#5083,#5084));
#1631=EDGE_LOOP('',(#5085,#5086,#5087,#5088));
#1632=EDGE_LOOP('',(#5089,#5090,#5091,#5092));
#1633=EDGE_LOOP('',(#5093,#5094,#5095,#5096));
#1634=EDGE_LOOP('',(#5097));
#1981=LINE('',#11144,#2314);
#1982=LINE('',#11146,#2315);
#1983=LINE('',#11148,#2316);
#1984=LINE('',#11149,#2317);
#1985=LINE('',#11152,#2318);
#1986=LINE('',#11154,#2319);
#1987=LINE('',#11155,#2320);
#1988=LINE('',#11158,#2321);
#1989=LINE('',#11160,#2322);
#1990=LINE('',#11161,#2323);
#1991=LINE('',#11164,#2324);
#1992=LINE('',#11166,#2325);
#1993=LINE('',#11167,#2326);
#1994=LINE('',#11170,#2327);
#1995=LINE('',#11172,#2328);
#1996=LINE('',#11173,#2329);
#1997=LINE('',#11175,#2330);
#1998=LINE('',#11176,#2331);
#1999=LINE('',#11184,#2332);
#2000=LINE('',#11188,#2333);
#2001=LINE('',#11192,#2334);
#2314=VECTOR('',#8694,1.);
#2315=VECTOR('',#8695,1.);
#2316=VECTOR('',#8696,1.);
#2317=VECTOR('',#8697,1.);
#2318=VECTOR('',#8700,1.);
#2319=VECTOR('',#8701,1.);
#2320=VECTOR('',#8702,1.);
#2321=VECTOR('',#8705,1.);
#2322=VECTOR('',#8706,1.);
#2323=VECTOR('',#8707,1.);
#2324=VECTOR('',#8710,1.);
#2325=VECTOR('',#8711,1.);
#2326=VECTOR('',#8712,1.);
#2327=VECTOR('',#8715,1.);
#2328=VECTOR('',#8716,1.);
#2329=VECTOR('',#8717,1.);
#2330=VECTOR('',#8720,1.);
#2331=VECTOR('',#8721,1.);
#2332=VECTOR('',#8732,0.185);
#2333=VECTOR('',#8737,0.2);
#2334=VECTOR('',#8742,0.1625);
#2735=CIRCLE('',#7116,0.17);
#2736=CIRCLE('',#7118,0.1954);
#2737=CIRCLE('',#7120,0.1954);
#2738=CIRCLE('',#7122,0.125);
#3166=VERTEX_POINT('',#11142);
#3167=VERTEX_POINT('',#11143);
#3168=VERTEX_POINT('',#11145);
#3169=VERTEX_POINT('',#11147);
#3170=VERTEX_POINT('',#11151);
#3171=VERTEX_POINT('',#11153);
#3172=VERTEX_POINT('',#11157);
#3173=VERTEX_POINT('',#11159);
#3174=VERTEX_POINT('',#11163);
#3175=VERTEX_POINT('',#11165);
#3176=VERTEX_POINT('',#11169);
#3177=VERTEX_POINT('',#11171);
#3178=VERTEX_POINT('',#11179);
#3179=VERTEX_POINT('',#11182);
#3180=VERTEX_POINT('',#11186);
#3181=VERTEX_POINT('',#11190);
#3819=EDGE_CURVE('',#3166,#3167,#1981,.T.);
#3820=EDGE_CURVE('',#3166,#3168,#1982,.T.);
#3821=EDGE_CURVE('',#3168,#3169,#1983,.T.);
#3822=EDGE_CURVE('',#3167,#3169,#1984,.T.);
#3823=EDGE_CURVE('',#3170,#3166,#1985,.T.);
#3824=EDGE_CURVE('',#3170,#3171,#1986,.T.);
#3825=EDGE_CURVE('',#3171,#3168,#1987,.T.);
#3826=EDGE_CURVE('',#3172,#3170,#1988,.T.);
#3827=EDGE_CURVE('',#3172,#3173,#1989,.T.);
#3828=EDGE_CURVE('',#3173,#3171,#1990,.T.);
#3829=EDGE_CURVE('',#3174,#3172,#1991,.T.);
#3830=EDGE_CURVE('',#3174,#3175,#1992,.T.);
#3831=EDGE_CURVE('',#3175,#3173,#1993,.T.);
#3832=EDGE_CURVE('',#3176,#3174,#1994,.T.);
#3833=EDGE_CURVE('',#3176,#3177,#1995,.T.);
#3834=EDGE_CURVE('',#3177,#3175,#1996,.T.);
#3835=EDGE_CURVE('',#3167,#3176,#1997,.T.);
#3836=EDGE_CURVE('',#3169,#3177,#1998,.T.);
#3837=EDGE_CURVE('',#3178,#3178,#2735,.T.);
#3838=EDGE_CURVE('',#3179,#3179,#2736,.T.);
#3839=EDGE_CURVE('',#3179,#3178,#1999,.T.);
#3840=EDGE_CURVE('',#3180,#3180,#2737,.F.);
#3841=EDGE_CURVE('',#3180,#3179,#2000,.T.);
#3842=EDGE_CURVE('',#3181,#3181,#2738,.T.);
#3843=EDGE_CURVE('',#3181,#3180,#2001,.T.);
#5048=ORIENTED_EDGE('',*,*,#3819,.F.);
#5049=ORIENTED_EDGE('',*,*,#3820,.T.);
#5050=ORIENTED_EDGE('',*,*,#3821,.T.);
#5051=ORIENTED_EDGE('',*,*,#3822,.F.);
#5052=ORIENTED_EDGE('',*,*,#3823,.F.);
#5053=ORIENTED_EDGE('',*,*,#3824,.T.);
#5054=ORIENTED_EDGE('',*,*,#3825,.T.);
#5055=ORIENTED_EDGE('',*,*,#3820,.F.);
#5056=ORIENTED_EDGE('',*,*,#3826,.F.);
#5057=ORIENTED_EDGE('',*,*,#3827,.T.);
#5058=ORIENTED_EDGE('',*,*,#3828,.T.);
#5059=ORIENTED_EDGE('',*,*,#3824,.F.);
#5060=ORIENTED_EDGE('',*,*,#3829,.F.);
#5061=ORIENTED_EDGE('',*,*,#3830,.T.);
#5062=ORIENTED_EDGE('',*,*,#3831,.T.);
#5063=ORIENTED_EDGE('',*,*,#3827,.F.);
#5064=ORIENTED_EDGE('',*,*,#3832,.F.);
#5065=ORIENTED_EDGE('',*,*,#3833,.T.);
#5066=ORIENTED_EDGE('',*,*,#3834,.T.);
#5067=ORIENTED_EDGE('',*,*,#3830,.F.);
#5068=ORIENTED_EDGE('',*,*,#3835,.F.);
#5069=ORIENTED_EDGE('',*,*,#3822,.T.);
#5070=ORIENTED_EDGE('',*,*,#3836,.T.);
#5071=ORIENTED_EDGE('',*,*,#3833,.F.);
#5072=ORIENTED_EDGE('',*,*,#3836,.F.);
#5073=ORIENTED_EDGE('',*,*,#3821,.F.);
#5074=ORIENTED_EDGE('',*,*,#3825,.F.);
#5075=ORIENTED_EDGE('',*,*,#3828,.F.);
#5076=ORIENTED_EDGE('',*,*,#3831,.F.);
#5077=ORIENTED_EDGE('',*,*,#3834,.F.);
#5078=ORIENTED_EDGE('',*,*,#3837,.F.);
#5079=ORIENTED_EDGE('',*,*,#3819,.T.);
#5080=ORIENTED_EDGE('',*,*,#3835,.T.);
#5081=ORIENTED_EDGE('',*,*,#3832,.T.);
#5082=ORIENTED_EDGE('',*,*,#3829,.T.);
#5083=ORIENTED_EDGE('',*,*,#3826,.T.);
#5084=ORIENTED_EDGE('',*,*,#3823,.T.);
#5085=ORIENTED_EDGE('',*,*,#3838,.F.);
#5086=ORIENTED_EDGE('',*,*,#3839,.T.);
#5087=ORIENTED_EDGE('',*,*,#3837,.T.);
#5088=ORIENTED_EDGE('',*,*,#3839,.F.);
#5089=ORIENTED_EDGE('',*,*,#3840,.F.);
#5090=ORIENTED_EDGE('',*,*,#3841,.T.);
#5091=ORIENTED_EDGE('',*,*,#3838,.T.);
#5092=ORIENTED_EDGE('',*,*,#3841,.F.);
#5093=ORIENTED_EDGE('',*,*,#3842,.F.);
#5094=ORIENTED_EDGE('',*,*,#3843,.T.);
#5095=ORIENTED_EDGE('',*,*,#3840,.T.);
#5096=ORIENTED_EDGE('',*,*,#3843,.F.);
#5097=ORIENTED_EDGE('',*,*,#3842,.T.);
#5650=CYLINDRICAL_SURFACE('',#7119,0.1954);
#5935=ADVANCED_FACE('',(#1129),#806,.F.);
#5936=ADVANCED_FACE('',(#1130),#807,.F.);
#5937=ADVANCED_FACE('',(#1131),#808,.F.);
#5938=ADVANCED_FACE('',(#1132),#809,.F.);
#5939=ADVANCED_FACE('',(#1133),#810,.F.);
#5940=ADVANCED_FACE('',(#1134),#811,.F.);
#5941=ADVANCED_FACE('',(#1135),#812,.F.);
#5942=ADVANCED_FACE('',(#1136,#648),#813,.T.);
#5943=ADVANCED_FACE('',(#1137),#300,.T.);
#5944=ADVANCED_FACE('',(#1138),#5650,.T.);
#5945=ADVANCED_FACE('',(#1139),#301,.T.);
#5946=ADVANCED_FACE('',(#1140),#814,.T.);
#6101=CLOSED_SHELL('',(#5935,#5936,#5937,#5938,#5939,#5940,#5941,#5942,
#5943,#5944,#5945,#5946));
#7107=AXIS2_PLACEMENT_3D('',#11140,#8690,#8691);
#7108=AXIS2_PLACEMENT_3D('',#11141,#8692,#8693);
#7109=AXIS2_PLACEMENT_3D('',#11150,#8698,#8699);
#7110=AXIS2_PLACEMENT_3D('',#11156,#8703,#8704);
#7111=AXIS2_PLACEMENT_3D('',#11162,#8708,#8709);
#7112=AXIS2_PLACEMENT_3D('',#11168,#8713,#8714);
#7113=AXIS2_PLACEMENT_3D('',#11174,#8718,#8719);
#7114=AXIS2_PLACEMENT_3D('',#11177,#8722,#8723);
#7115=AXIS2_PLACEMENT_3D('',#11178,#8724,#8725);
#7116=AXIS2_PLACEMENT_3D('',#11180,#8726,#8727);
#7117=AXIS2_PLACEMENT_3D('',#11181,#8728,#8729);
#7118=AXIS2_PLACEMENT_3D('',#11183,#8730,#8731);
#7119=AXIS2_PLACEMENT_3D('',#11185,#8733,#8734);
#7120=AXIS2_PLACEMENT_3D('',#11187,#8735,#8736);
#7121=AXIS2_PLACEMENT_3D('',#11189,#8738,#8739);
#7122=AXIS2_PLACEMENT_3D('',#11191,#8740,#8741);
#7123=AXIS2_PLACEMENT_3D('',#11193,#8743,#8744);
#8690=DIRECTION('axis',(0.,0.,1.));
#8691=DIRECTION('refdir',(1.,0.,0.));
#8692=DIRECTION('center_axis',(0.866025403784439,0.,-0.5));
#8693=DIRECTION('ref_axis',(0.5,0.,0.866025403784439));
#8694=DIRECTION('',(0.5,0.,0.866025403784439));
#8695=DIRECTION('',(0.,-1.,0.));
#8696=DIRECTION('',(0.5,0.,0.866025403784439));
#8697=DIRECTION('',(0.,-1.,0.));
#8698=DIRECTION('center_axis',(1.20185167898973E-16,0.,-1.));
#8699=DIRECTION('ref_axis',(1.,0.,1.20185167898973E-16));
#8700=DIRECTION('',(1.,0.,1.20185167898973E-16));
#8701=DIRECTION('',(0.,-1.,0.));
#8702=DIRECTION('',(1.,0.,1.20185167898973E-16));
#8703=DIRECTION('center_axis',(-0.866025403784439,0.,-0.5));
#8704=DIRECTION('ref_axis',(0.5,0.,-0.866025403784439));
#8705=DIRECTION('',(0.5,0.,-0.866025403784439));
#8706=DIRECTION('',(0.,-1.,0.));
#8707=DIRECTION('',(0.5,0.,-0.866025403784439));
#8708=DIRECTION('center_axis',(-0.866025403784439,0.,0.5));
#8709=DIRECTION('ref_axis',(-0.5,0.,-0.866025403784439));
#8710=DIRECTION('',(-0.5,0.,-0.866025403784439));
#8711=DIRECTION('',(0.,-1.,0.));
#8712=DIRECTION('',(-0.5,0.,-0.866025403784439));
#8713=DIRECTION('center_axis',(-2.40370335797945E-16,0.,1.));
#8714=DIRECTION('ref_axis',(-1.,0.,-2.40370335797945E-16));
#8715=DIRECTION('',(-1.,0.,-2.40370335797945E-16));
#8716=DIRECTION('',(0.,-1.,0.));
#8717=DIRECTION('',(-1.,0.,-2.40370335797945E-16));
#8718=DIRECTION('center_axis',(0.866025403784439,0.,0.5));
#8719=DIRECTION('ref_axis',(-0.5,0.,0.866025403784439));
#8720=DIRECTION('',(-0.5,0.,0.866025403784439));
#8721=DIRECTION('',(-0.5,0.,0.866025403784439));
#8722=DIRECTION('center_axis',(0.,-1.,0.));
#8723=DIRECTION('ref_axis',(0.,0.,-1.));
#8724=DIRECTION('center_axis',(0.,1.,0.));
#8725=DIRECTION('ref_axis',(0.,0.,1.));
#8726=DIRECTION('center_axis',(0.,-1.,0.));
#8727=DIRECTION('ref_axis',(1.,0.,0.));
#8728=DIRECTION('center_axis',(0.,-1.,0.));
#8729=DIRECTION('ref_axis',(1.,0.,0.));
#8730=DIRECTION('center_axis',(0.,-1.,0.));
#8731=DIRECTION('ref_axis',(1.,0.,0.));
#8732=DIRECTION('',(0.707106781186548,0.707106781186547,8.65956056235494E-17));
#8733=DIRECTION('center_axis',(0.,-1.,0.));
#8734=DIRECTION('ref_axis',(1.,0.,0.));
#8735=DIRECTION('center_axis',(0.,1.,0.));
#8736=DIRECTION('ref_axis',(1.,0.,0.));
#8737=DIRECTION('',(0.,1.,0.));
#8738=DIRECTION('center_axis',(0.,1.,0.));
#8739=DIRECTION('ref_axis',(1.,0.,0.));
#8740=DIRECTION('center_axis',(0.,-1.,0.));
#8741=DIRECTION('ref_axis',(1.,0.,0.));
#8742=DIRECTION('',(-0.707106781186548,0.707106781186547,-8.65956056235494E-17));
#8743=DIRECTION('center_axis',(0.,-1.,0.));
#8744=DIRECTION('ref_axis',(0.,0.,-1.));
#11140=CARTESIAN_POINT('',(0.,0.,0.));
#11141=CARTESIAN_POINT('Origin',(0.0577350269189626,0.,-0.1));
#11142=CARTESIAN_POINT('',(0.0577350269189626,0.,-0.1));
#11143=CARTESIAN_POINT('',(0.115470053837925,0.,0.));
#11144=CARTESIAN_POINT('',(0.0934187836487032,0.,-0.0381939203391614));
#11145=CARTESIAN_POINT('',(0.0577350269189626,-0.2,-0.1));
#11146=CARTESIAN_POINT('',(0.0577350269189626,0.,-0.1));
#11147=CARTESIAN_POINT('',(0.115470053837925,-0.2,0.));
#11148=CARTESIAN_POINT('',(0.115470053837925,-0.2,0.));
#11149=CARTESIAN_POINT('',(0.115470053837925,0.,0.));
#11150=CARTESIAN_POINT('Origin',(-0.0577350269189626,0.,-0.1));
#11151=CARTESIAN_POINT('',(-0.0577350269189626,0.,-0.1));
#11152=CARTESIAN_POINT('',(0.0561324865405187,0.,-0.1));
#11153=CARTESIAN_POINT('',(-0.0577350269189626,-0.2,-0.1));
#11154=CARTESIAN_POINT('',(-0.0577350269189626,0.,-0.1));
#11155=CARTESIAN_POINT('',(0.0577350269189626,-0.2,-0.1));
#11156=CARTESIAN_POINT('Origin',(-0.115470053837925,0.,-1.38777878078145E-17));
#11157=CARTESIAN_POINT('',(-0.115470053837925,0.,-1.41410031829988E-17));
#11158=CARTESIAN_POINT('',(-0.0797862971081845,0.,-0.0618060796608387));
#11159=CARTESIAN_POINT('',(-0.115470053837925,-0.2,-1.38777878078145E-17));
#11160=CARTESIAN_POINT('',(-0.115470053837925,0.,-1.41410031829988E-17));
#11161=CARTESIAN_POINT('',(-0.0577350269189626,-0.2,-0.1));
#11162=CARTESIAN_POINT('Origin',(-0.0577350269189626,0.,0.1));
#11163=CARTESIAN_POINT('',(-0.0577350269189626,0.,0.1));
#11164=CARTESIAN_POINT('',(-0.0509187836487033,0.,0.111806079660839));
#11165=CARTESIAN_POINT('',(-0.0577350269189626,-0.2,0.1));
#11166=CARTESIAN_POINT('',(-0.0577350269189626,0.,0.1));
#11167=CARTESIAN_POINT('',(-0.115470053837925,-0.2,-1.41410031829988E-17));
#11168=CARTESIAN_POINT('Origin',(0.0577350269189626,0.,0.1));
#11169=CARTESIAN_POINT('',(0.0577350269189626,0.,0.1));
#11170=CARTESIAN_POINT('',(0.113867513459481,0.,0.1));
#11171=CARTESIAN_POINT('',(0.0577350269189626,-0.2,0.1));
#11172=CARTESIAN_POINT('',(0.0577350269189626,0.,0.1));
#11173=CARTESIAN_POINT('',(-0.0577350269189626,-0.2,0.1));
#11174=CARTESIAN_POINT('Origin',(0.115470053837925,0.,0.));
#11175=CARTESIAN_POINT('',(0.122286297108185,0.,-0.0118060796608386));
#11176=CARTESIAN_POINT('',(0.0577350269189626,-0.2,0.1));
#11177=CARTESIAN_POINT('Origin',(0.,-0.2,0.));
#11178=CARTESIAN_POINT('Origin',(0.17,0.,0.));
#11179=CARTESIAN_POINT('',(-0.17,-8.67361737988404E-18,-2.0818995585505E-17));
#11180=CARTESIAN_POINT('Origin',(0.,0.,0.));
#11181=CARTESIAN_POINT('Origin',(0.,-0.015,0.));
#11182=CARTESIAN_POINT('',(-0.1954,-0.0254,-2.39295984553393E-17));
#11183=CARTESIAN_POINT('Origin',(0.,-0.0254,0.));
#11184=CARTESIAN_POINT('',(-0.185,-0.015,-2.2655965784226E-17));
#11185=CARTESIAN_POINT('Origin',(0.,-0.2775,0.));
#11186=CARTESIAN_POINT('',(-0.1954,-0.5296,2.39295984553393E-17));
#11187=CARTESIAN_POINT('Origin',(0.,-0.5296,0.));
#11188=CARTESIAN_POINT('',(-0.1954,-0.2775,-2.39295984553393E-17));
#11189=CARTESIAN_POINT('Origin',(0.,-0.5625,0.));
#11190=CARTESIAN_POINT('',(-0.125,-0.6,-1.53080849893419E-17));
#11191=CARTESIAN_POINT('Origin',(0.,-0.6,0.));
#11192=CARTESIAN_POINT('',(-0.1625,-0.5625,-1.99005104861445E-17));
#11193=CARTESIAN_POINT('Origin',(0.,-0.6,0.));
#11852=UNCERTAINTY_MEASURE_WITH_UNIT(LENGTH_MEASURE(0.001),#11917,
'DISTANCE_ACCURACY_VALUE',
'Maximum model space distance between geometric entities at asserted c
onnectivities');
#11869=UNCERTAINTY_MEASURE_WITH_UNIT(LENGTH_MEASURE(0.001),#11917,
'DISTANCE_ACCURACY_VALUE',
'Maximum model space distance between geometric entities at asserted c
onnectivities');
#11899=(
GEOMETRIC_REPRESENTATION_CONTEXT(3)
GLOBAL_UNCERTAINTY_ASSIGNED_CONTEXT((#11852))
GLOBAL_UNIT_ASSIGNED_CONTEXT((#11917,#11919,#11920))
REPRESENTATION_CONTEXT('','3D')
);
#11916=(
GEOMETRIC_REPRESENTATION_CONTEXT(3)
GLOBAL_UNCERTAINTY_ASSIGNED_CONTEXT((#11869))
GLOBAL_UNIT_ASSIGNED_CONTEXT((#11917,#11919,#11920))
REPRESENTATION_CONTEXT('','3D')
);
#11917=(
LENGTH_UNIT()
NAMED_UNIT(*)
SI_UNIT(.CENTI.,.METRE.)
);
#11919=(
NAMED_UNIT(*)
PLANE_ANGLE_UNIT()
SI_UNIT($,.RADIAN.)
);
#11920=(
NAMED_UNIT(*)
SI_UNIT($,.STERADIAN.)
SOLID_ANGLE_UNIT()
);
#11950=SHAPE_DEFINITION_REPRESENTATION(#12001,#12108);
#12001=PRODUCT_DEFINITION_SHAPE('',$,#12155);
#12108=SHAPE_REPRESENTATION('',(#7107),#11899);
#12125=PRODUCT_DEFINITION_CONTEXT('part definition',#12265,'design');
#12155=PRODUCT_DEFINITION('Socket Set Screw - M4x6',
'Socket Set Screw - M4x6',#12201,#12125);
#12201=PRODUCT_DEFINITION_FORMATION('',$,#12296);
#12265=APPLICATION_CONTEXT(
'Core Data for Automotive Mechanical Design Process');
#12266=PRODUCT_CONTEXT('part definition',#12265,'mechanical');
#12296=PRODUCT('Socket Set Screw - M4x6','Socket Set Screw - M4x6',
'Socket Set Screw - M4x6',(#12266));
#12376=COLOUR_RGB('Black',0.12,0.14,0.17);
#12377=FILL_AREA_STYLE_COLOUR('',#12376);
#12378=FILL_AREA_STYLE('',(#12377));
#12379=SURFACE_STYLE_FILL_AREA(#12378);
#12380=SURFACE_SIDE_STYLE('',(#12379));
#12381=SURFACE_STYLE_USAGE(.BOTH.,#12380);
#12382=PRESENTATION_STYLE_ASSIGNMENT((#12381));
ENDSEC;
END-ISO-10303-21;
